ISO-10303-21;
HEADER;
FILE_DESCRIPTION (('STEP AP214'),
    '1' );
FILE_NAME ('Washer.step',
    '2026-10-06T09:00:30',
    ( '' ),
    ( '' ),
    'SwSTEP 2.0',
    'SolidWorks 2020',
    '' );
FILE_SCHEMA (( 'AUTOMOTIVE_DESIGN' ));
ENDSEC;

DATA;
#56=ORIENTED_EDGE ( 'NONE', *, *, #13467, .F. ) ;
#481=ORIENTED_EDGE ( 'NONE', *, *, #2473, .T. ) ;
#593=ORIENTED_EDGE ( 'NONE', *, *, #25979, .T. ) ;
#621=DIRECTION ( 'NONE',  ( -1.000000000000000000, -0.000000000000000000, -6.771000000000000128E-12 ) ) ;
#707=ORIENTED_EDGE ( 'NONE', *, *, #25056, .T. ) ;
#715=ORIENTED_EDGE ( 'NONE', *, *, #21453, .F. ) ;
#740=EDGE_CURVE ( 'NONE', #4043, #4187, #12790, .T. ) ;
#761=ORIENTED_EDGE ( 'NONE', *, *, #22188, .T. ) ;
#789=ORIENTED_EDGE ( 'NONE', *, *, #21453, .T. ) ;
#900=EDGE_LOOP ( 'NONE', ( #20816, #30735 ) ) ;
#923=CARTESIAN_POINT ( 'NONE',  ( -12.29999999970000069, -27.00000000000000000, -28.40000000001083791 ) ) ;
#1126=CARTESIAN_POINT ( 'NONE',  ( -10.69999999969999926, -27.00000000000000000, -28.40000000000000213 ) ) ;
#1162=CARTESIAN_POINT ( 'NONE',  ( -12.29999999970000069, -27.00000000000000000, -28.40000000001083791 ) ) ;
#1175=ORIENTED_EDGE ( 'NONE', *, *, #14244, .F. ) ;
#1190=EDGE_LOOP ( 'NONE', ( #5983, #12137 ) ) ;
#1235=CIRCLE ( 'NONE', #17813, 6.000000000000001776 ) ;
#1396=ORIENTED_EDGE ( 'NONE', *, *, #18688, .T. ) ;
#1499=CARTESIAN_POINT ( 'NONE',  ( -10.69999999967832949, -27.41951581582461372, -31.60007023061346842 ) ) ;
#1545=CIRCLE ( 'NONE', #4053, 6.000000000000001776 ) ;
#1651=CARTESIAN_POINT ( 'NONE',  ( -10.69999999968267090, -28.96604956106295603, -30.95933451744668830 ) ) ;
#1797=CARTESIAN_POINT ( 'NONE',  ( -12.29999999999139781, -26.16240677005030335, -31.51671256534945087 ) ) ;
#1863=EDGE_CURVE ( 'NONE', #11498, #6120, #24556, .T. ) ;
#2054=( NAMED_UNIT ( * ) PLANE_ANGLE_UNIT ( ) SI_UNIT ( $, .RADIAN. ) );
#2115=CARTESIAN_POINT ( 'NONE',  ( -10.69999999969716065, -23.80000000000000071, -28.81986915868696641 ) ) ;
#2196=ADVANCED_FACE ( 'NONE', ( #26328 ), #14682, .F. ) ;
#2464=EDGE_CURVE ( 'NONE', #27585, #21516, #11649, .T. ) ;
#2473=EDGE_CURVE ( 'NONE', #7813, #4043, #1545, .T. ) ;
#2627=CARTESIAN_POINT ( 'NONE',  ( 0.000000000000000000, 0.000000000000000000, 0.000000000000000000 ) ) ;
#2769=CARTESIAN_POINT ( 'NONE',  ( -12.30000000044999986, -30.20000000000000284, -28.40000000001083791 ) ) ;
#2888=CARTESIAN_POINT ( 'NONE',  ( -11.49999999969999998, -27.00000000000000000, -28.40000000000541647 ) ) ;
#2950=APPLICATION_CONTEXT ( 'automotive_design' ) ;
#2963=FACE_OUTER_BOUND ( 'NONE', #28015, .T. ) ;
#3005=CARTESIAN_POINT ( 'NONE',  ( -11.50000000044500048, -20.99999999999999645, -28.40000000000541647 ) ) ;
#3062=UNCERTAINTY_MEASURE_WITH_UNIT (LENGTH_MEASURE( 1.000000000000000082E-05 ), #18882, 'distance_accuracy_value', 'NONE');
#3078=ADVANCED_FACE ( 'NONE', ( #17186 ), #16042, .T. ) ;
#3085=CARTESIAN_POINT ( 'NONE',  ( -10.69999999895494192, -23.79999999999999716, -28.40000000000000213 ) ) ;
#3119=PRODUCT ( 'Washer', 'Washer', '', ( #13822 ) ) ;
#3182=STYLED_ITEM ( 'NONE', ( #21246 ), #6893 ) ;
#3248=ORIENTED_EDGE ( 'NONE', *, *, #9098, .T. ) ;
#3279=VERTEX_POINT ( 'NONE', #15296 ) ;
#3296=PRODUCT_DEFINITION ( 'UNKNOWN', '', #24408, #25091 ) ;
#3571=DIRECTION ( 'NONE',  ( 0.6087614290090099800, -0.7933533402910131205, 4.134191582186808379E-12 ) ) ;
#3800=ORIENTED_EDGE ( 'NONE', *, *, #10791, .T. ) ;
#3912=VECTOR ( 'NONE', #30304, 1000.000000000000114 ) ;
#4043=VERTEX_POINT ( 'NONE', #11318 ) ;
#4053=AXIS2_PLACEMENT_3D ( 'NONE', #13984, #11311, #14138 ) ;
#4149=CARTESIAN_POINT ( 'NONE',  ( -12.29999999990142534, -25.03345049608028106, -30.95893389568501419 ) ) ;
#4187=VERTEX_POINT ( 'NONE', #17110 ) ;
#4377=DIRECTION ( 'NONE',  ( -1.000000000000000000, 0.000000000000000000, -6.771000000000000128E-12 ) ) ;
#4411=SURFACE_STYLE_FILL_AREA ( #6344 ) ;
#4463=CARTESIAN_POINT ( 'NONE',  ( -12.29999999975682812, -23.88328743466139059, -29.23759322996053811 ) ) ;
#4476=CARTESIAN_POINT ( 'NONE',  ( -10.69999999969714999, -30.19999999999998863, -28.82059031327837673 ) ) ;
#4528=CARTESIAN_POINT ( 'NONE',  ( -10.69999999969999926, -27.00000000000000000, -28.40000000000000213 ) ) ;
#4767=CIRCLE ( 'NONE', #18319, 5.400000000370001274 ) ;
#5023=DIRECTION ( 'NONE',  ( -1.000000000000000000, 0.000000000000000000, -6.771000000000000128E-12 ) ) ;
#5127=CARTESIAN_POINT ( 'NONE',  ( -11.83960380690999870, -27.00000000000000000, -28.40000000000771863 ) ) ;
#5348=CARTESIAN_POINT ( 'NONE',  ( -12.29999999970000069, -27.00000000000000000, -28.40000000001083436 ) ) ;
#5423=( GEOMETRIC_REPRESENTATION_CONTEXT ( 3 ) GLOBAL_UNCERTAINTY_ASSIGNED_CONTEXT ( ( #12542 ) ) GLOBAL_UNIT_ASSIGNED_CONTEXT ( ( #21407, #2054, #13259 ) ) REPRESENTATION_CONTEXT ( 'NONE', 'WORKASPACE' ) );
#5478=LINE ( 'NONE', #20118, #6262 ) ;
#5546=AXIS2_PLACEMENT_3D ( 'NONE', #1126, #4377, #21068 ) ;
#5884=CARTESIAN_POINT ( 'NONE',  ( -11.50000000044500048, -30.20000000000000284, -28.40000000000542002 ) ) ;
#5926=CARTESIAN_POINT ( 'NONE',  ( -15.44356573478999906, -26.99999999999999289, -28.40000000003211866 ) ) ;
#5983=ORIENTED_EDGE ( 'NONE', *, *, #22188, .F. ) ;
#6093=CARTESIAN_POINT ( 'NONE',  ( -10.69999999969999926, -27.00000000000000000, -28.40000000000000213 ) ) ;
#6095=VERTEX_POINT ( 'NONE', #25060 ) ;
#6103=SHAPE_DEFINITION_REPRESENTATION ( #27251, #8955 ) ;
#6120=VERTEX_POINT ( 'NONE', #25694 ) ;
#6262=VECTOR ( 'NONE', #17732, 1000.000000000000114 ) ;
#6344=FILL_AREA_STYLE ('',( #28777 ) ) ;
#6500=ORIENTED_EDGE ( 'NONE', *, *, #740, .F. ) ;
#6854=DIRECTION ( 'NONE',  ( -1.000000000000000000, 1.662859514859999923E-15, -6.790296706416999781E-12 ) ) ;
#6858=DIRECTION ( 'NONE',  ( 1.000000000000000000, -1.634095982650525115E-15, 6.790302532597771964E-12 ) ) ;
#6867=DIRECTION ( 'NONE',  ( -1.000000000000000000, 1.467383017310000131E-15, -6.771000000000000128E-12 ) ) ;
#6893=ADVANCED_BREP_SHAPE_REPRESENTATION ( '', ( #11447, #17722 ), #22285 ) ;
#6917=SURFACE_STYLE_USAGE ( .BOTH. , #25972 ) ;
#6980=DIRECTION ( 'NONE',  ( 1.000000000000000000, -1.634095982650525115E-15, 6.790302532597771964E-12 ) ) ;
#7062=CARTESIAN_POINT ( 'NONE',  ( -11.50000000044500048, -23.79999999999999716, -28.40000000000541647 ) ) ;
#7068=B_SPLINE_CURVE_WITH_KNOTS ( 'NONE', 3,
 ( #21141, #28213, #4463, #8696, #15791, #4149, #14063, #1797, #11388, #13744, #30736, #30436, #13590, #30898, #28059, #20986, #11076, #18615 ),
 .UNSPECIFIED., .F., .F.,
 ( 4, 2, 2, 2, 2, 2, 2, 2, 4 ),
 ( 0.000000000000000000, 0.1250000000000003053, 0.2500000000000006106, 0.3750000000000001665, 0.5000000000000002220, 0.6250000000000002220, 0.7500000000000001110, 0.8750000000000001110, 1.000000000000000000 ),
 .UNSPECIFIED. ) ;
#7086=CIRCLE ( 'NONE', #26668, 3.200000000000001510 ) ;
#7200=ORIENTED_EDGE ( 'NONE', *, *, #13556, .F. ) ;
#7234=EDGE_CURVE ( 'NONE', #16248, #8336, #14548, .T. ) ;
#7682=ORIENTED_EDGE ( 'NONE', *, *, #13467, .T. ) ;
#7740=CONICAL_SURFACE ( 'NONE', #30872, 1.303225372841144925, 0.9162978572969998625 ) ;
#7800=CARTESIAN_POINT ( 'NONE',  ( -10.69999999895494192, -27.00000000000000000, -28.40000000000000213 ) ) ;
#7813=VERTEX_POINT ( 'NONE', #15140 ) ;
#7932=MECHANICAL_DESIGN_GEOMETRIC_PRESENTATION_REPRESENTATION('',(#19498),#5423);
#8015=CLOSED_SHELL ( 'NONE', ( #24255, #27972, #27471, #13113, #3078, #26307, #2196, #19760, #19880 ) ) ;
#8245=AXIS2_PLACEMENT_3D ( 'NONE', #16271, #14081, #14392 ) ;
#8336=VERTEX_POINT ( 'NONE', #20104 ) ;
#8447=AXIS2_PLACEMENT_3D ( 'NONE', #1162, #20199, #10455 ) ;
#8696=CARTESIAN_POINT ( 'NONE',  ( -12.29999999981408720, -24.20388355726637641, -30.01158073719771480 ) ) ;
#8754=CARTESIAN_POINT ( 'NONE',  ( -15.44356573478999906, -26.99999999999999289, -28.40000000003218972 ) ) ;
#8757=FACE_OUTER_BOUND ( 'NONE', #18696, .T. ) ;
#8763=CARTESIAN_POINT ( 'NONE',  ( -11.49999999969999998, -27.00000000000000000, -28.40000000000541647 ) ) ;
#8808=VERTEX_POINT ( 'NONE', #3085 ) ;
#8928=PLANE ( 'NONE',  #20798 ) ;
#8955=SHAPE_REPRESENTATION ( 'Washer', ( #17722 ), #22285 ) ;
#9098=EDGE_CURVE ( 'NONE', #3279, #4043, #11111, .T. ) ;
#9179=CARTESIAN_POINT ( 'NONE',  ( -10.69999999967889259, -27.83695679439218651, -31.51688268319167463 ) ) ;
#9219=VECTOR ( 'NONE', #22205, 1000.000000000000000 ) ;
#9273=CARTESIAN_POINT ( 'NONE',  ( -12.29999999970000069, -32.40000000036999950, -28.40000000001083080 ) ) ;
#9429=PRESENTATION_STYLE_ASSIGNMENT (( #6917 ) ) ;
#9449=EDGE_CURVE ( 'NONE', #8336, #16248, #7068, .T. ) ;
#9885=ORIENTED_EDGE ( 'NONE', *, *, #9449, .F. ) ;
#9978=DIRECTION ( 'NONE',  ( 0.000000000000000000, -1.000000000000000000, 0.000000000000000000 ) ) ;
#9995=VECTOR ( 'NONE', #25095, 1000.000000000000000 ) ;
#10025=( NAMED_UNIT ( * ) SI_UNIT ( $, .STERADIAN. ) SOLID_ANGLE_UNIT ( ) );
#10095=LINE ( 'NONE', #3005, #9219 ) ;
#10172=APPLICATION_CONTEXT ( 'automotive_design' ) ;
#10178=( NAMED_UNIT ( * ) SI_UNIT ( $, .STERADIAN. ) SOLID_ANGLE_UNIT ( ) );
#10314=UNCERTAINTY_MEASURE_WITH_UNIT (LENGTH_MEASURE( 1.000000000000000082E-05 ), #12528, 'distance_accuracy_value', 'NONE');
#10455=DIRECTION ( 'NONE',  ( 0.000000000000000000, -1.000000000000000000, 0.000000000000000000 ) ) ;
#10791=EDGE_CURVE ( 'NONE', #6120, #3279, #29512, .T. ) ;
#10988=DIRECTION ( 'NONE',  ( 0.000000000000000000, -1.000000000000000000, 0.000000000000000000 ) ) ;
#11075=ORIENTED_EDGE ( 'NONE', *, *, #7234, .T. ) ;
#11076=CARTESIAN_POINT ( 'NONE',  ( -12.30000000041591512, -30.20000000000000284, -28.81887902048947225 ) ) ;
#11111=LINE ( 'NONE', #20707, #3912 ) ;
#11311=DIRECTION ( 'NONE',  ( -1.000000000000000000, 1.662859514859999923E-15, -6.790296706416999781E-12 ) ) ;
#11318=CARTESIAN_POINT ( 'NONE',  ( -11.83960380690193404, -32.88057757210000176, -29.59113702762771680 ) ) ;
#11371=ORIENTED_EDGE ( 'NONE', *, *, #18688, .F. ) ;
#11388=CARTESIAN_POINT ( 'NONE',  ( -12.30000000002208438, -26.58112097952136565, -31.60000000001083365 ) ) ;
#11447=MANIFOLD_SOLID_BREP ( 'PartBody', #8015 ) ;
#11498=VERTEX_POINT ( 'NONE', #9273 ) ;
#11649=CIRCLE ( 'NONE', #5546, 6.000000000000001776 ) ;
#12046=AXIS2_PLACEMENT_3D ( 'NONE', #23405, #23560, #14105 ) ;
#12137=ORIENTED_EDGE ( 'NONE', *, *, #2464, .F. ) ;
#12213=MECHANICAL_DESIGN_GEOMETRIC_PRESENTATION_REPRESENTATION('',(#3182),#30330);
#12220=SURFACE_STYLE_USAGE ( .BOTH. , #14599 ) ;
#12262=ORIENTED_EDGE ( 'NONE', *, *, #22228, .T. ) ;
#12319=CARTESIAN_POINT ( 'NONE',  ( -15.44356573478999906, -26.99999999999999289, -28.40000000003218972 ) ) ;
#12378=FILL_AREA_STYLE ('',( #30691 ) ) ;
#12520=DIRECTION ( 'NONE',  ( -1.000000000000000000, 0.000000000000000000, -6.771000000000000128E-12 ) ) ;
#12528=( LENGTH_UNIT ( ) NAMED_UNIT ( * ) SI_UNIT ( .MILLI., .METRE. ) );
#12542=UNCERTAINTY_MEASURE_WITH_UNIT (LENGTH_MEASURE( 1.000000000000000082E-05 ), #21407, 'distance_accuracy_value', 'NONE');
#12556=PLANE ( 'NONE',  #15673 ) ;
#12674=CARTESIAN_POINT ( 'NONE',  ( -10.69999999969999926, -20.99999999999999645, -28.39999999999999858 ) ) ;
#12790=CIRCLE ( 'NONE', #14570, 6.000000000000001776 ) ;
#12988=DIRECTION ( 'NONE',  ( 0.000000000000000000, -1.000000000000000000, 0.000000000000000000 ) ) ;
#13012=DIRECTION ( 'NONE',  ( 1.331100139797737888E-15, 1.000000000000000000, 0.000000000000000000 ) ) ;
#13113=ADVANCED_FACE ( 'NONE', ( #25764 ), #25588, .T. ) ;
#13172=DIRECTION ( 'NONE',  ( -1.000000000000000000, 0.000000000000000000, -6.771000000000000128E-12 ) ) ;
#13259=( NAMED_UNIT ( * ) SI_UNIT ( $, .STERADIAN. ) SOLID_ANGLE_UNIT ( ) );
#13414=ORIENTED_EDGE ( 'NONE', *, *, #2473, .F. ) ;
#13467=EDGE_CURVE ( 'NONE', #6095, #16248, #27443, .T. ) ;
#13556=EDGE_CURVE ( 'NONE', #8808, #6095, #23001, .T. ) ;
#13590=CARTESIAN_POINT ( 'NONE',  ( -12.30000000021392736, -28.96654950391973671, -30.95893389568501419 ) ) ;
#13744=CARTESIAN_POINT ( 'NONE',  ( -12.30000000008458549, -27.41887902047864500, -31.60000000001083365 ) ) ;
#13822=PRODUCT_CONTEXT ( 'NONE', #10172, 'mechanical' ) ;
#13919=CARTESIAN_POINT ( 'NONE',  ( -10.69999999968107041, -25.38784894342604659, -31.19578670632331097 ) ) ;
#13923=FACE_OUTER_BOUND ( 'NONE', #26332, .T. ) ;
#13984=CARTESIAN_POINT ( 'NONE',  ( -11.83960380690999870, -27.00000000000000000, -28.40000000000771863 ) ) ;
#14015=DIRECTION ( 'NONE',  ( 0.000000000000000000, 0.000000000000000000, 1.000000000000000000 ) ) ;
#14063=CARTESIAN_POINT ( 'NONE',  ( -12.29999999993107096, -25.38841926281313377, -31.19611644274446860 ) ) ;
#14078=CARTESIAN_POINT ( 'NONE',  ( -10.69999999968668192, -29.55943383853203699, -30.36614888214831609 ) ) ;
#14081=DIRECTION ( 'NONE',  ( -1.000000000000000000, 0.000000000000000000, -6.771000000000000128E-12 ) ) ;
#14105=DIRECTION ( 'NONE',  ( 0.000000000000000000, -1.000000000000000000, 0.000000000000000000 ) ) ;
#14114=CARTESIAN_POINT ( 'NONE',  ( -10.69999999969999926, -33.00000000000000000, -28.40000000000000213 ) ) ;
#14138=DIRECTION ( 'NONE',  ( 1.734723475976806503E-15, 1.000000000000000000, 0.000000000000000000 ) ) ;
#14244=EDGE_CURVE ( 'NONE', #11498, #4187, #27643, .T. ) ;
#14313=LINE ( 'NONE', #7062, #30332 ) ;
#14392=DIRECTION ( 'NONE',  ( 0.000000000000000000, 1.000000000000000000, 0.000000000000000000 ) ) ;
#14548=CIRCLE ( 'NONE', #12046, 3.199999999250000560 ) ;
#14570=AXIS2_PLACEMENT_3D ( 'NONE', #27787, #6854, #23088 ) ;
#14599=SURFACE_SIDE_STYLE ('',( #21095 ) ) ;
#14682=CYLINDRICAL_SURFACE ( 'NONE', #30242, 3.200000000000001510 ) ;
#14781=CARTESIAN_POINT ( 'NONE',  ( -11.50000000044500048, -33.00000000000000000, -28.40000000000542002 ) ) ;
#15140=CARTESIAN_POINT ( 'NONE',  ( -11.83960380747999963, -20.99999999999999645, -28.40000000000771863 ) ) ;
#15296=CARTESIAN_POINT ( 'NONE',  ( -12.29999999969274072, -32.29251981524999593, -29.47202332494083521 ) ) ;
#15450=AXIS2_PLACEMENT_3D ( 'NONE', #5348, #19674, #29257 ) ;
#15673=AXIS2_PLACEMENT_3D ( 'NONE', #923, #621, #22164 ) ;
#15727=ORIENTED_EDGE ( 'NONE', *, *, #10791, .F. ) ;
#15785=AXIS2_PLACEMENT_3D ( 'NONE', #5127, #6867, #21823 ) ;
#15791=CARTESIAN_POINT ( 'NONE',  ( -12.29999999984293346, -24.44106610432582727, -30.36654950393056396 ) ) ;
#16042=CONICAL_SURFACE ( 'NONE', #21583, 1.303225372841142260, 0.9162978572969998625 ) ;
#16248=VERTEX_POINT ( 'NONE', #2769 ) ;
#16271=CARTESIAN_POINT ( 'NONE',  ( -11.49999999969999998, -27.00000000000000000, -28.40000000000541647 ) ) ;
#16527=ORIENTED_EDGE ( 'NONE', *, *, #1863, .T. ) ;
#16570=DIRECTION ( 'NONE',  ( 1.347073341475313442E-12, -0.9800962620158550909, -0.1985228379369698981 ) ) ;
#16652=DIRECTION ( 'NONE',  ( -1.000000000000000000, 0.000000000000000000, -6.771000000000000128E-12 ) ) ;
#16734=EDGE_LOOP ( 'NONE', ( #3248, #21624, #1175, #25313 ) ) ;
#16789=CIRCLE ( 'NONE', #15785, 6.000000000000001776 ) ;
#16895=FACE_OUTER_BOUND ( 'NONE', #21915, .T. ) ;
#17110=CARTESIAN_POINT ( 'NONE',  ( -11.83960380747999963, -33.00000000000000000, -28.40000000000771863 ) ) ;
#17186=FACE_OUTER_BOUND ( 'NONE', #23305, .T. ) ;
#17402=( NAMED_UNIT ( * ) PLANE_ANGLE_UNIT ( ) SI_UNIT ( $, .RADIAN. ) );
#17722=AXIS2_PLACEMENT_3D ( 'NONE', #2627, #14015, #29203 ) ;
#17732=DIRECTION ( 'NONE',  ( 0.6087614290090099800, 0.7933533402910131205, 4.134802762626407668E-12 ) ) ;
#17813=AXIS2_PLACEMENT_3D ( 'NONE', #6093, #13172, #19958 ) ;
#17821=ORIENTED_EDGE ( 'NONE', *, *, #1863, .F. ) ;
#18093=EDGE_LOOP ( 'NONE', ( #9885, #26170 ) ) ;
#18120=AXIS2_PLACEMENT_3D ( 'NONE', #8763, #18372, #28274 ) ;
#18319=AXIS2_PLACEMENT_3D ( 'NONE', #24377, #26727, #30992 ) ;
#18372=DIRECTION ( 'NONE',  ( -1.000000000000000000, 0.000000000000000000, -6.771000000000000128E-12 ) ) ;
#18475=CARTESIAN_POINT ( 'NONE',  ( -10.69999999968908355, -29.79578670632410820, -30.01215105656972071 ) ) ;
#18615=CARTESIAN_POINT ( 'NONE',  ( -12.30000000044999986, -30.20000000000000284, -28.40000000001083791 ) ) ;
#18629=CARTESIAN_POINT ( 'NONE',  ( -10.69999999967833659, -26.58048418417539338, -31.59992976938654508 ) ) ;
#18688=EDGE_CURVE ( 'NONE', #8808, #8336, #14313, .T. ) ;
#18696=EDGE_LOOP ( 'NONE', ( #25550, #789, #31033, #17821 ) ) ;
#18719=( NAMED_UNIT ( * ) PLANE_ANGLE_UNIT ( ) SI_UNIT ( $, .RADIAN. ) );
#18769=DIRECTION ( 'NONE',  ( 0.000000000000000000, -1.000000000000000000, 0.000000000000000000 ) ) ;
#18809=ORIENTED_EDGE ( 'NONE', *, *, #9098, .F. ) ;
#18882=( LENGTH_UNIT ( ) NAMED_UNIT ( * ) SI_UNIT ( .MILLI., .METRE. ) );
#18940=CARTESIAN_POINT ( 'NONE',  ( -10.69999999969433446, -23.88311731680927608, -29.23695679439294537 ) ) ;
#19498=STYLED_ITEM ( 'NONE', ( #9429 ), #11447 ) ;
#19674=DIRECTION ( 'NONE',  ( -1.000000000000000000, 0.000000000000000000, -6.771000000000000128E-12 ) ) ;
#19760=ADVANCED_FACE ( 'NONE', ( #24832, #2963 ), #12556, .T. ) ;
#19880=ADVANCED_FACE ( 'NONE', ( #30334 ), #20898, .F. ) ;
#19958=DIRECTION ( 'NONE',  ( 0.000000000000000000, -1.000000000000000000, 0.000000000000000000 ) ) ;
#20031=EDGE_CURVE ( 'NONE', #6095, #8808, #7086, .T. ) ;
#20104=CARTESIAN_POINT ( 'NONE',  ( -12.29999999970000069, -23.80000000074999988, -28.40000000001083791 ) ) ;
#20118=CARTESIAN_POINT ( 'NONE',  ( 304364.2709390003583, 396649.6701459999895, -28.39999793263759997 ) ) ;
#20199=DIRECTION ( 'NONE',  ( -1.000000000000000000, 0.000000000000000000, -6.771000000000000128E-12 ) ) ;
#20249=CARTESIAN_POINT ( 'NONE',  ( 304364.2709390003583, -396703.6701459999895, -28.39999793294318664 ) ) ;
#20564=DIRECTION ( 'NONE',  ( 1.000000000000000000, -1.408687696619999864E-15, 6.771000000000000128E-12 ) ) ;
#20580=FACE_OUTER_BOUND ( 'NONE', #1190, .T. ) ;
#20631=ORIENTED_EDGE ( 'NONE', *, *, #29108, .T. ) ;
#20707=CARTESIAN_POINT ( 'NONE',  ( 304364.2709395335405, -388808.3216389999725, -78777.77829863908119 ) ) ;
#20798=AXIS2_PLACEMENT_3D ( 'NONE', #4528, #25782, #10988 ) ;
#20816=ORIENTED_EDGE ( 'NONE', *, *, #20031, .T. ) ;
#20898=CYLINDRICAL_SURFACE ( 'NONE', #18120, 3.200000000000001510 ) ;
#20921=ORIENTED_EDGE ( 'NONE', *, *, #25979, .F. ) ;
#20986=CARTESIAN_POINT ( 'NONE',  ( -12.30000000038183039, -30.11671256533862007, -29.23759322996053100 ) ) ;
#21001=CARTESIAN_POINT ( 'NONE',  ( -10.69999999895494192, -23.79999999999999716, -28.40000000000000213 ) ) ;
#21068=DIRECTION ( 'NONE',  ( 0.000000000000000000, -1.000000000000000000, 0.000000000000000000 ) ) ;
#21095=SURFACE_STYLE_FILL_AREA ( #12378 ) ;
#21141=CARTESIAN_POINT ( 'NONE',  ( -12.29999999970000069, -23.80000000074999988, -28.40000000001083791 ) ) ;
#21154=CARTESIAN_POINT ( 'NONE',  ( -10.69999999967889615, -26.16298946189287022, -31.51701243199215341 ) ) ;
#21246=PRESENTATION_STYLE_ASSIGNMENT (( #12220 ) ) ;
#21407=( LENGTH_UNIT ( ) NAMED_UNIT ( * ) SI_UNIT ( .MILLI., .METRE. ) );
#21453=EDGE_CURVE ( 'NONE', #4187, #7813, #16789, .T. ) ;
#21516=VERTEX_POINT ( 'NONE', #12674 ) ;
#21583=AXIS2_PLACEMENT_3D ( 'NONE', #12319, #6980, #16570 ) ;
#21624=ORIENTED_EDGE ( 'NONE', *, *, #740, .T. ) ;
#21823=DIRECTION ( 'NONE',  ( 1.445602896647338719E-15, 1.000000000000000000, 0.000000000000000000 ) ) ;
#21830=SHAPE_REPRESENTATION_RELATIONSHIP ( 'NONE' , 'NONE' ,  #8955, #6893 ) ;
#21915=EDGE_LOOP ( 'NONE', ( #20921, #29867, #20631, #715 ) ) ;
#22164=DIRECTION ( 'NONE',  ( 0.000000000000000000, -1.000000000000000000, 0.000000000000000000 ) ) ;
#22188=EDGE_CURVE ( 'NONE', #21516, #27585, #1235, .T. ) ;
#22205=DIRECTION ( 'NONE',  ( -1.000000000000000000, 0.000000000000000000, -6.771000000000000128E-12 ) ) ;
#22228=EDGE_CURVE ( 'NONE', #6120, #7813, #5478, .T. ) ;
#22243=DIRECTION ( 'NONE',  ( -1.000000000000000000, 0.000000000000000000, -6.771000000000000128E-12 ) ) ;
#22285=( GEOMETRIC_REPRESENTATION_CONTEXT ( 3 ) GLOBAL_UNCERTAINTY_ASSIGNED_CONTEXT ( ( #3062 ) ) GLOBAL_UNIT_ASSIGNED_CONTEXT ( ( #18882, #17402, #10025 ) ) REPRESENTATION_CONTEXT ( 'NONE', 'WORKASPACE' ) );
#22645=EDGE_LOOP ( 'NONE', ( #28227, #56, #7200, #1396 ) ) ;
#23001=B_SPLINE_CURVE_WITH_KNOTS ( 'NONE', 3,
 ( #21001, #2115, #18940, #30751, #23055, #23529, #13919, #21154, #18629, #1499, #9179, #28226, #1651, #14078, #18475, #30450, #4476, #26036 ),
 .UNSPECIFIED., .F., .F.,
 ( 4, 2, 2, 2, 2, 2, 2, 2, 4 ),
 ( 0.000000000000000000, 0.1249999999999993061, 0.2499999999999986122, 0.3749999999999986122, 0.4999999999999986677, 0.6249999999999987788, 0.7499999999999991118, 0.8749999999999995559, 1.000000000000000000 ),
 .UNSPECIFIED. ) ;
#23055=CARTESIAN_POINT ( 'NONE',  ( -10.69999999968668725, -24.44066548255720761, -30.36604956106650377 ) ) ;
#23088=DIRECTION ( 'NONE',  ( 1.734723475976806503E-15, 1.000000000000000000, 0.000000000000000000 ) ) ;
#23305=EDGE_LOOP ( 'NONE', ( #18809, #15727, #12262, #481 ) ) ;
#23405=CARTESIAN_POINT ( 'NONE',  ( -12.29999999970000069, -27.00000000000000000, -28.40000000001083436 ) ) ;
#23412=DIRECTION ( 'NONE',  ( -1.347073341475313442E-12, 0.9800962620158550909, 0.1985228379369698981 ) ) ;
#23529=CARTESIAN_POINT ( 'NONE',  ( -10.69999999968266913, -25.03385111784779227, -30.95943383852850062 ) ) ;
#23560=DIRECTION ( 'NONE',  ( -1.000000000000000000, 0.000000000000000000, -6.771000000000000128E-12 ) ) ;
#23584=FACE_BOUND ( 'NONE', #900, .T. ) ;
#24255=ADVANCED_FACE ( 'NONE', ( #16895 ), #28850, .T. ) ;
#24293=EDGE_LOOP ( 'NONE', ( #11075, #11371, #30633, #7682 ) ) ;
#24377=CARTESIAN_POINT ( 'NONE',  ( -12.29999999970000069, -27.00000000000000000, -28.40000000001083436 ) ) ;
#24381=LINE ( 'NONE', #14781, #28314 ) ;
#24408=PRODUCT_DEFINITION_FORMATION_WITH_SPECIFIED_SOURCE ( 'ANY', '', #3119, .NOT_KNOWN. ) ;
#24556=CIRCLE ( 'NONE', #8447, 5.400000000370001274 ) ;
#24832=FACE_BOUND ( 'NONE', #18093, .T. ) ;
#25033=ORIENTED_EDGE ( 'NONE', *, *, #29108, .F. ) ;
#25056=EDGE_CURVE ( 'NONE', #3279, #11498, #4767, .T. ) ;
#25060=CARTESIAN_POINT ( 'NONE',  ( -10.69999999969999926, -30.19999999925000012, -28.40000000000000213 ) ) ;
#25091=PRODUCT_DEFINITION_CONTEXT ( 'detailed design', #2950, 'design' ) ;
#25095=DIRECTION ( 'NONE',  ( -1.000000000000000000, 0.000000000000000000, -6.771000000000000128E-12 ) ) ;
#25313=ORIENTED_EDGE ( 'NONE', *, *, #25056, .F. ) ;
#25550=ORIENTED_EDGE ( 'NONE', *, *, #14244, .T. ) ;
#25588=CONICAL_SURFACE ( 'NONE', #29078, 1.303225372841142260, 0.9162978572969998625 ) ;
#25694=CARTESIAN_POINT ( 'NONE',  ( -12.29999999970000069, -21.59999999962999695, -28.40000000001083791 ) ) ;
#25764=FACE_OUTER_BOUND ( 'NONE', #16734, .T. ) ;
#25782=DIRECTION ( 'NONE',  ( -1.000000000000000000, -0.000000000000000000, -6.771000000000000128E-12 ) ) ;
#25972=SURFACE_SIDE_STYLE ('',( #4411 ) ) ;
#25979=EDGE_CURVE ( 'NONE', #27585, #4187, #24381, .T. ) ;
#26036=CARTESIAN_POINT ( 'NONE',  ( -10.69999999969999926, -30.19999999925000012, -28.40000000000000213 ) ) ;
#26170=ORIENTED_EDGE ( 'NONE', *, *, #7234, .F. ) ;
#26172=CARTESIAN_POINT ( 'NONE',  ( -11.49999999969999998, -27.00000000000000000, -28.40000000000541647 ) ) ;
#26307=ADVANCED_FACE ( 'NONE', ( #23584, #20580 ), #8928, .F. ) ;
#26310=COLOUR_RGB ( '', 0.08235294, 0.09019608, 0.10196078) ;
#26328=FACE_OUTER_BOUND ( 'NONE', #24293, .T. ) ;
#26332=EDGE_LOOP ( 'NONE', ( #25033, #761, #593, #6500, #13414 ) ) ;
#26668=AXIS2_PLACEMENT_3D ( 'NONE', #7800, #12520, #12988 ) ;
#26727=DIRECTION ( 'NONE',  ( -1.000000000000000000, 0.000000000000000000, -6.771000000000000128E-12 ) ) ;
#27037=COLOUR_RGB ( '', 0.08235294, 0.09019608, 0.10196078) ;
#27069=VECTOR ( 'NONE', #3571, 1000.000000000000114 ) ;
#27251=PRODUCT_DEFINITION_SHAPE ( 'NONE', 'NONE',  #3296 ) ;
#27443=LINE ( 'NONE', #5884, #9995 ) ;
#27471=ADVANCED_FACE ( 'NONE', ( #8757 ), #7740, .T. ) ;
#27585=VERTEX_POINT ( 'NONE', #14114 ) ;
#27643=LINE ( 'NONE', #20249, #27069 ) ;
#27787=CARTESIAN_POINT ( 'NONE',  ( -11.83960380690999870, -27.00000000000000000, -28.40000000000771863 ) ) ;
#27972=ADVANCED_FACE ( 'NONE', ( #13923 ), #28229, .T. ) ;
#28015=EDGE_LOOP ( 'NONE', ( #3800, #707, #16527 ) ) ;
#28059=CARTESIAN_POINT ( 'NONE',  ( -12.30000000031408725, -29.79611644273363424, -30.01158073719770414 ) ) ;
#28213=CARTESIAN_POINT ( 'NONE',  ( -12.29999999972841351, -23.79999999999999716, -28.81887902048947936 ) ) ;
#28226=CARTESIAN_POINT ( 'NONE',  ( -10.69999999968106863, -28.61220480028889668, -31.19591645512378975 ) ) ;
#28227=ORIENTED_EDGE ( 'NONE', *, *, #9449, .T. ) ;
#28229=CYLINDRICAL_SURFACE ( 'NONE', #8245, 6.000000000000001776 ) ;
#28274=DIRECTION ( 'NONE',  ( 0.000000000000000000, 1.000000000000000000, 0.000000000000000000 ) ) ;
#28314=VECTOR ( 'NONE', #5023, 1000.000000000000000 ) ;
#28777=FILL_AREA_STYLE_COLOUR ( '', #27037 ) ;
#28824=DIRECTION ( 'NONE',  ( -1.000000000000000000, 0.000000000000000000, -6.771000000000000128E-12 ) ) ;
#28850=CYLINDRICAL_SURFACE ( 'NONE', #29833, 6.000000000000001776 ) ;
#29078=AXIS2_PLACEMENT_3D ( 'NONE', #8754, #6858, #23412 ) ;
#29108=EDGE_CURVE ( 'NONE', #21516, #7813, #10095, .T. ) ;
#29203=DIRECTION ( 'NONE',  ( 1.000000000000000000, 0.000000000000000000, 0.000000000000000000 ) ) ;
#29257=DIRECTION ( 'NONE',  ( 0.000000000000000000, -1.000000000000000000, 0.000000000000000000 ) ) ;
#29512=CIRCLE ( 'NONE', #15450, 5.400000000370001274 ) ;
#29833=AXIS2_PLACEMENT_3D ( 'NONE', #2888, #22243, #9978 ) ;
#29867=ORIENTED_EDGE ( 'NONE', *, *, #2464, .T. ) ;
#30242=AXIS2_PLACEMENT_3D ( 'NONE', #26172, #28824, #18769 ) ;
#30304=DIRECTION ( 'NONE',  ( 0.6087614290101102110, -0.7775626432770559315, -0.1574987565968895831 ) ) ;
#30330=( GEOMETRIC_REPRESENTATION_CONTEXT ( 3 ) GLOBAL_UNCERTAINTY_ASSIGNED_CONTEXT ( ( #10314 ) ) GLOBAL_UNIT_ASSIGNED_CONTEXT ( ( #12528, #18719, #10178 ) ) REPRESENTATION_CONTEXT ( 'NONE', 'WORKASPACE' ) );
#30332=VECTOR ( 'NONE', #16652, 1000.000000000000000 ) ;
#30334=FACE_OUTER_BOUND ( 'NONE', #22645, .T. ) ;
#30436=CARTESIAN_POINT ( 'NONE',  ( -12.30000000018107009, -28.61158073718687689, -31.19611644274446149 ) ) ;
#30450=CARTESIAN_POINT ( 'NONE',  ( -10.69999999969433269, -30.11701243199135902, -29.23701053811106476 ) ) ;
#30633=ORIENTED_EDGE ( 'NONE', *, *, #20031, .F. ) ;
#30691=FILL_AREA_STYLE_COLOUR ( '', #26310 ) ;
#30735=ORIENTED_EDGE ( 'NONE', *, *, #13556, .T. ) ;
#30736=CARTESIAN_POINT ( 'NONE',  ( -12.30000000011639827, -27.83759322994970375, -31.51671256534945087 ) ) ;
#30751=CARTESIAN_POINT ( 'NONE',  ( -10.69999999968908355, -24.20408354487524605, -30.01220480028783655 ) ) ;
#30872=AXIS2_PLACEMENT_3D ( 'NONE', #5926, #20564, #13012 ) ;
#30898=CARTESIAN_POINT ( 'NONE',  ( -12.30000000028043416, -29.55893389567417273, -30.36654950393055685 ) ) ;
#30992=DIRECTION ( 'NONE',  ( 0.000000000000000000, -1.000000000000000000, 0.000000000000000000 ) ) ;
#31033=ORIENTED_EDGE ( 'NONE', *, *, #22228, .F. ) ;
ENDSEC;
END-ISO-10303-21;
